ISO-10303-21;
HEADER;
/* Generated by software containing ST-Developer
 * from STEP Tools, Inc. (www.steptools.com) 
 */

FILE_DESCRIPTION(
/* description */ ('Union bypass pipe loop'),
/* implementation_level */ '2;1');

FILE_NAME(
/* name */ 'Hex Nut - M8.step',
/* time_stamp */ '2026-10-27T21:00:29-07:00',
/* author */ (''),
/* organization */ (''),
/* preprocessor_version */ 'ST-DEVELOPER v20.2',
/* originating_system */ 'Autodesk Translation Framework v15.17.0.0',
/* authorisation */ '');

FILE_SCHEMA (('AUTOMOTIVE_DESIGN { 1 0 10303 214 3 1 1 }'));
ENDSEC;

DATA;
#10=MECHANICAL_DESIGN_GEOMETRIC_PRESENTATION_REPRESENTATION('',(#470),#10095);
#339=(
BOUNDED_CURVE()
B_SPLINE_CURVE(2,(#9615,#9616,#9617),.UNSPECIFIED.,.F.,.F.)
B_SPLINE_CURVE_WITH_KNOTS((3,3),(0.14973948338295,0.97160236658079),
 .UNSPECIFIED.)
CURVE()
GEOMETRIC_REPRESENTATION_ITEM()
RATIONAL_B_SPLINE_CURVE((1.07140024848292,1.23714644374248,1.07140024848292))
REPRESENTATION_ITEM('')
);
#340=(
BOUNDED_CURVE()
B_SPLINE_CURVE(2,(#9619,#9620,#9621),.UNSPECIFIED.,.F.,.F.)
B_SPLINE_CURVE_WITH_KNOTS((3,3),(0.14973948338295,0.971602366580789),
 .UNSPECIFIED.)
CURVE()
GEOMETRIC_REPRESENTATION_ITEM()
RATIONAL_B_SPLINE_CURVE((1.07140024848292,1.23714644374248,1.07140024848292))
REPRESENTATION_ITEM('')
);
#341=(
BOUNDED_CURVE()
B_SPLINE_CURVE(2,(#9626,#9627,#9628),.UNSPECIFIED.,.F.,.F.)
B_SPLINE_CURVE_WITH_KNOTS((3,3),(0.14973948338295,0.97160236658079),
 .UNSPECIFIED.)
CURVE()
GEOMETRIC_REPRESENTATION_ITEM()
RATIONAL_B_SPLINE_CURVE((1.07140024848292,1.23714644374248,1.07140024848292))
REPRESENTATION_ITEM('')
);
#342=(
BOUNDED_CURVE()
B_SPLINE_CURVE(2,(#9630,#9631,#9632),.UNSPECIFIED.,.F.,.F.)
B_SPLINE_CURVE_WITH_KNOTS((3,3),(0.14973948338295,0.97160236658079),
 .UNSPECIFIED.)
CURVE()
GEOMETRIC_REPRESENTATION_ITEM()
RATIONAL_B_SPLINE_CURVE((1.07140024848292,1.23714644374248,1.07140024848292))
REPRESENTATION_ITEM('')
);
#343=(
BOUNDED_CURVE()
B_SPLINE_CURVE(2,(#9634,#9635,#9636),.UNSPECIFIED.,.F.,.F.)
B_SPLINE_CURVE_WITH_KNOTS((3,3),(0.14973948338295,0.971602366580789),
 .UNSPECIFIED.)
CURVE()
GEOMETRIC_REPRESENTATION_ITEM()
RATIONAL_B_SPLINE_CURVE((1.07140024848292,1.23714644374248,1.07140024848292))
REPRESENTATION_ITEM('')
);
#344=(
BOUNDED_CURVE()
B_SPLINE_CURVE(2,(#9637,#9638,#9639),.UNSPECIFIED.,.F.,.F.)
B_SPLINE_CURVE_WITH_KNOTS((3,3),(0.14973948338295,0.97160236658079),
 .UNSPECIFIED.)
CURVE()
GEOMETRIC_REPRESENTATION_ITEM()
RATIONAL_B_SPLINE_CURVE((1.07140024848292,1.23714644374248,1.07140024848292))
REPRESENTATION_ITEM('')
);
#345=(
BOUNDED_CURVE()
B_SPLINE_CURVE(2,(#9646,#9647,#9648),.UNSPECIFIED.,.F.,.F.)
B_SPLINE_CURVE_WITH_KNOTS((3,3),(0.14973948338295,0.97160236658079),
 .UNSPECIFIED.)
CURVE()
GEOMETRIC_REPRESENTATION_ITEM()
RATIONAL_B_SPLINE_CURVE((1.07140024848292,1.23714644374248,1.07140024848292))
REPRESENTATION_ITEM('')
);
#346=(
BOUNDED_CURVE()
B_SPLINE_CURVE(2,(#9650,#9651,#9652),.UNSPECIFIED.,.F.,.F.)
B_SPLINE_CURVE_WITH_KNOTS((3,3),(0.14973948338295,0.97160236658079),
 .UNSPECIFIED.)
CURVE()
GEOMETRIC_REPRESENTATION_ITEM()
RATIONAL_B_SPLINE_CURVE((1.07140024848292,1.23714644374248,1.07140024848292))
REPRESENTATION_ITEM('')
);
#347=(
BOUNDED_CURVE()
B_SPLINE_CURVE(2,(#9654,#9655,#9656),.UNSPECIFIED.,.F.,.F.)
B_SPLINE_CURVE_WITH_KNOTS((3,3),(0.14973948338295,0.971602366580789),
 .UNSPECIFIED.)
CURVE()
GEOMETRIC_REPRESENTATION_ITEM()
RATIONAL_B_SPLINE_CURVE((1.07140024848292,1.23714644374248,1.07140024848292))
REPRESENTATION_ITEM('')
);
#348=(
BOUNDED_CURVE()
B_SPLINE_CURVE(2,(#9658,#9659,#9660),.UNSPECIFIED.,.F.,.F.)
B_SPLINE_CURVE_WITH_KNOTS((3,3),(0.14973948338295,0.97160236658079),
 .UNSPECIFIED.)
CURVE()
GEOMETRIC_REPRESENTATION_ITEM()
RATIONAL_B_SPLINE_CURVE((1.07140024848292,1.23714644374248,1.07140024848292))
REPRESENTATION_ITEM('')
);
#349=(
BOUNDED_CURVE()
B_SPLINE_CURVE(2,(#9662,#9663,#9664),.UNSPECIFIED.,.F.,.F.)
B_SPLINE_CURVE_WITH_KNOTS((3,3),(0.14973948338295,0.97160236658079),
 .UNSPECIFIED.)
CURVE()
GEOMETRIC_REPRESENTATION_ITEM()
RATIONAL_B_SPLINE_CURVE((1.07140024848292,1.23714644374248,1.07140024848292))
REPRESENTATION_ITEM('')
);
#350=(
BOUNDED_CURVE()
B_SPLINE_CURVE(2,(#9665,#9666,#9667),.UNSPECIFIED.,.F.,.F.)
B_SPLINE_CURVE_WITH_KNOTS((3,3),(0.14973948338295,0.971602366580789),
 .UNSPECIFIED.)
CURVE()
GEOMETRIC_REPRESENTATION_ITEM()
RATIONAL_B_SPLINE_CURVE((1.07140024848292,1.23714644374248,1.07140024848292))
REPRESENTATION_ITEM('')
);
#367=CONICAL_SURFACE('',#6461,0.734027674973257,1.0471975511966);
#368=CONICAL_SURFACE('',#6463,0.734027674973257,1.0471975511966);
#406=SHAPE_REPRESENTATION_RELATIONSHIP('SRR','None',#10275,#438);
#438=ADVANCED_BREP_SHAPE_REPRESENTATION('',(#499),#10087);
#470=STYLED_ITEM('',(#10507),#499);
#499=MANIFOLD_SOLID_BREP('Body1',#5544);
#624=FACE_BOUND('',#1546,.T.);
#625=FACE_BOUND('',#1548,.T.);
#773=PLANE('',#6465);
#774=PLANE('',#6466);
#775=PLANE('',#6467);
#776=PLANE('',#6471);
#777=PLANE('',#6472);
#778=PLANE('',#6473);
#779=PLANE('',#6474);
#780=PLANE('',#6475);
#1091=FACE_OUTER_BOUND('',#1536,.T.);
#1092=FACE_OUTER_BOUND('',#1537,.T.);
#1093=FACE_OUTER_BOUND('',#1538,.T.);
#1094=FACE_OUTER_BOUND('',#1539,.T.);
#1095=FACE_OUTER_BOUND('',#1540,.T.);
#1096=FACE_OUTER_BOUND('',#1541,.T.);
#1097=FACE_OUTER_BOUND('',#1542,.T.);
#1098=FACE_OUTER_BOUND('',#1543,.T.);
#1099=FACE_OUTER_BOUND('',#1544,.T.);
#1100=FACE_OUTER_BOUND('',#1545,.T.);
#1101=FACE_OUTER_BOUND('',#1547,.T.);
#1536=EDGE_LOOP('',(#4760,#4761,#4762,#4763,#4764,#4765,#4766,#4767,#4768));
#1537=EDGE_LOOP('',(#4769,#4770,#4771,#4772,#4773,#4774,#4775,#4776,#4777));
#1538=EDGE_LOOP('',(#4778,#4779,#4780,#4781));
#1539=EDGE_LOOP('',(#4782,#4783,#4784,#4785));
#1540=EDGE_LOOP('',(#4786,#4787,#4788,#4789));
#1541=EDGE_LOOP('',(#4790,#4791,#4792,#4793));
#1542=EDGE_LOOP('',(#4794,#4795,#4796,#4797));
#1543=EDGE_LOOP('',(#4798,#4799,#4800,#4801));
#1544=EDGE_LOOP('',(#4802,#4803,#4804,#4805));
#1545=EDGE_LOOP('',(#4806));
#1546=EDGE_LOOP('',(#4807));
#1547=EDGE_LOOP('',(#4808));
#1548=EDGE_LOOP('',(#4809));
#1886=LINE('',#9623,#2262);
#1887=LINE('',#9644,#2263);
#1888=LINE('',#9669,#2264);
#1889=LINE('',#9670,#2265);
#1890=LINE('',#9672,#2266);
#1891=LINE('',#9674,#2267);
#1892=LINE('',#9679,#2268);
#1893=LINE('',#9682,#2269);
#1894=LINE('',#9684,#2270);
#2262=VECTOR('',#7996,0.734027674973257);
#2263=VECTOR('',#8003,0.734027674973257);
#2264=VECTOR('',#8006,1.);
#2265=VECTOR('',#8007,1.);
#2266=VECTOR('',#8010,1.);
#2267=VECTOR('',#8013,1.);
#2268=VECTOR('',#8018,0.4);
#2269=VECTOR('',#8023,1.);
#2270=VECTOR('',#8026,1.);
#2595=CIRCLE('',#6462,0.6175);
#2596=CIRCLE('',#6464,0.6175);
#2597=CIRCLE('',#6469,0.338975);
#2598=CIRCLE('',#6470,0.338975);
#2964=VERTEX_POINT('',#9613);
#2965=VERTEX_POINT('',#9614);
#2966=VERTEX_POINT('',#9618);
#2967=VERTEX_POINT('',#9622);
#2968=VERTEX_POINT('',#9625);
#2969=VERTEX_POINT('',#9629);
#2970=VERTEX_POINT('',#9633);
#2971=VERTEX_POINT('',#9641);
#2972=VERTEX_POINT('',#9643);
#2973=VERTEX_POINT('',#9645);
#2974=VERTEX_POINT('',#9649);
#2975=VERTEX_POINT('',#9653);
#2976=VERTEX_POINT('',#9657);
#2977=VERTEX_POINT('',#9661);
#2978=VERTEX_POINT('',#9676);
#2979=VERTEX_POINT('',#9678);
#3578=EDGE_CURVE('',#2964,#2965,#339,.T.);
#3579=EDGE_CURVE('',#2966,#2964,#340,.T.);
#3580=EDGE_CURVE('',#2966,#2967,#1886,.T.);
#3581=EDGE_CURVE('',#2967,#2967,#2595,.T.);
#3582=EDGE_CURVE('',#2968,#2966,#341,.T.);
#3583=EDGE_CURVE('',#2969,#2968,#342,.T.);
#3584=EDGE_CURVE('',#2970,#2969,#343,.T.);
#3585=EDGE_CURVE('',#2965,#2970,#344,.T.);
#3586=EDGE_CURVE('',#2971,#2971,#2596,.T.);
#3587=EDGE_CURVE('',#2971,#2972,#1887,.T.);
#3588=EDGE_CURVE('',#2973,#2972,#345,.T.);
#3589=EDGE_CURVE('',#2974,#2973,#346,.T.);
#3590=EDGE_CURVE('',#2975,#2974,#347,.T.);
#3591=EDGE_CURVE('',#2976,#2975,#348,.T.);
#3592=EDGE_CURVE('',#2977,#2976,#349,.T.);
#3593=EDGE_CURVE('',#2972,#2977,#350,.T.);
#3594=EDGE_CURVE('',#2968,#2977,#1888,.T.);
#3595=EDGE_CURVE('',#2969,#2976,#1889,.T.);
#3596=EDGE_CURVE('',#2966,#2972,#1890,.T.);
#3597=EDGE_CURVE('',#2964,#2973,#1891,.T.);
#3598=EDGE_CURVE('',#2978,#2978,#2597,.F.);
#3599=EDGE_CURVE('',#2978,#2979,#1892,.T.);
#3600=EDGE_CURVE('',#2979,#2979,#2598,.F.);
#3601=EDGE_CURVE('',#2965,#2974,#1893,.T.);
#3602=EDGE_CURVE('',#2970,#2975,#1894,.T.);
#4760=ORIENTED_EDGE('',*,*,#3578,.F.);
#4761=ORIENTED_EDGE('',*,*,#3579,.F.);
#4762=ORIENTED_EDGE('',*,*,#3580,.T.);
#4763=ORIENTED_EDGE('',*,*,#3581,.F.);
#4764=ORIENTED_EDGE('',*,*,#3580,.F.);
#4765=ORIENTED_EDGE('',*,*,#3582,.F.);
#4766=ORIENTED_EDGE('',*,*,#3583,.F.);
#4767=ORIENTED_EDGE('',*,*,#3584,.F.);
#4768=ORIENTED_EDGE('',*,*,#3585,.F.);
#4769=ORIENTED_EDGE('',*,*,#3586,.F.);
#4770=ORIENTED_EDGE('',*,*,#3587,.T.);
#4771=ORIENTED_EDGE('',*,*,#3588,.F.);
#4772=ORIENTED_EDGE('',*,*,#3589,.F.);
#4773=ORIENTED_EDGE('',*,*,#3590,.F.);
#4774=ORIENTED_EDGE('',*,*,#3591,.F.);
#4775=ORIENTED_EDGE('',*,*,#3592,.F.);
#4776=ORIENTED_EDGE('',*,*,#3593,.F.);
#4777=ORIENTED_EDGE('',*,*,#3587,.F.);
#4778=ORIENTED_EDGE('',*,*,#3583,.T.);
#4779=ORIENTED_EDGE('',*,*,#3594,.T.);
#4780=ORIENTED_EDGE('',*,*,#3592,.T.);
#4781=ORIENTED_EDGE('',*,*,#3595,.F.);
#4782=ORIENTED_EDGE('',*,*,#3582,.T.);
#4783=ORIENTED_EDGE('',*,*,#3596,.T.);
#4784=ORIENTED_EDGE('',*,*,#3593,.T.);
#4785=ORIENTED_EDGE('',*,*,#3594,.F.);
#4786=ORIENTED_EDGE('',*,*,#3579,.T.);
#4787=ORIENTED_EDGE('',*,*,#3597,.T.);
#4788=ORIENTED_EDGE('',*,*,#3588,.T.);
#4789=ORIENTED_EDGE('',*,*,#3596,.F.);
#4790=ORIENTED_EDGE('',*,*,#3598,.F.);
#4791=ORIENTED_EDGE('',*,*,#3599,.T.);
#4792=ORIENTED_EDGE('',*,*,#3600,.T.);
#4793=ORIENTED_EDGE('',*,*,#3599,.F.);
#4794=ORIENTED_EDGE('',*,*,#3578,.T.);
#4795=ORIENTED_EDGE('',*,*,#3601,.T.);
#4796=ORIENTED_EDGE('',*,*,#3589,.T.);
#4797=ORIENTED_EDGE('',*,*,#3597,.F.);
#4798=ORIENTED_EDGE('',*,*,#3584,.T.);
#4799=ORIENTED_EDGE('',*,*,#3595,.T.);
#4800=ORIENTED_EDGE('',*,*,#3591,.T.);
#4801=ORIENTED_EDGE('',*,*,#3602,.F.);
#4802=ORIENTED_EDGE('',*,*,#3585,.T.);
#4803=ORIENTED_EDGE('',*,*,#3602,.T.);
#4804=ORIENTED_EDGE('',*,*,#3590,.T.);
#4805=ORIENTED_EDGE('',*,*,#3601,.F.);
#4806=ORIENTED_EDGE('',*,*,#3586,.T.);
#4807=ORIENTED_EDGE('',*,*,#3598,.T.);
#4808=ORIENTED_EDGE('',*,*,#3581,.T.);
#4809=ORIENTED_EDGE('',*,*,#3600,.F.);
#5176=CYLINDRICAL_SURFACE('',#6468,0.338975);
#5440=ADVANCED_FACE('',(#1091),#367,.T.);
#5441=ADVANCED_FACE('',(#1092),#368,.T.);
#5442=ADVANCED_FACE('',(#1093),#773,.T.);
#5443=ADVANCED_FACE('',(#1094),#774,.T.);
#5444=ADVANCED_FACE('',(#1095),#775,.T.);
#5445=ADVANCED_FACE('',(#1096),#5176,.F.);
#5446=ADVANCED_FACE('',(#1097),#776,.T.);
#5447=ADVANCED_FACE('',(#1098),#777,.T.);
#5448=ADVANCED_FACE('',(#1099),#778,.T.);
#5449=ADVANCED_FACE('',(#1100,#624),#779,.T.);
#5450=ADVANCED_FACE('',(#1101,#625),#780,.F.);
#5544=CLOSED_SHELL('',(#5440,#5441,#5442,#5443,#5444,#5445,#5446,#5447,
#5448,#5449,#5450));
#6460=AXIS2_PLACEMENT_3D('',#9611,#7992,#7993);
#6461=AXIS2_PLACEMENT_3D('',#9612,#7994,#7995);
#6462=AXIS2_PLACEMENT_3D('',#9624,#7997,#7998);
#6463=AXIS2_PLACEMENT_3D('',#9640,#7999,#8000);
#6464=AXIS2_PLACEMENT_3D('',#9642,#8001,#8002);
#6465=AXIS2_PLACEMENT_3D('',#9668,#8004,#8005);
#6466=AXIS2_PLACEMENT_3D('',#9671,#8008,#8009);
#6467=AXIS2_PLACEMENT_3D('',#9673,#8011,#8012);
#6468=AXIS2_PLACEMENT_3D('',#9675,#8014,#8015);
#6469=AXIS2_PLACEMENT_3D('',#9677,#8016,#8017);
#6470=AXIS2_PLACEMENT_3D('',#9680,#8019,#8020);
#6471=AXIS2_PLACEMENT_3D('',#9681,#8021,#8022);
#6472=AXIS2_PLACEMENT_3D('',#9683,#8024,#8025);
#6473=AXIS2_PLACEMENT_3D('',#9685,#8027,#8028);
#6474=AXIS2_PLACEMENT_3D('',#9686,#8029,#8030);
#6475=AXIS2_PLACEMENT_3D('',#9687,#8031,#8032);
#7992=DIRECTION('axis',(0.,0.,1.));
#7993=DIRECTION('refdir',(1.,0.,0.));
#7994=DIRECTION('center_axis',(0.,1.,0.));
#7995=DIRECTION('ref_axis',(1.,0.,0.));
#7996=DIRECTION('',(0.866025403784439,-0.5,1.06057523872491E-16));
#7997=DIRECTION('center_axis',(0.,-1.,0.));
#7998=DIRECTION('ref_axis',(1.,0.,0.));
#7999=DIRECTION('center_axis',(0.,-1.,0.));
#8000=DIRECTION('ref_axis',(1.,0.,0.));
#8001=DIRECTION('center_axis',(0.,1.,0.));
#8002=DIRECTION('ref_axis',(1.,0.,0.));
#8003=DIRECTION('',(-0.866025403784439,-0.5,-1.06057523872491E-16));
#8004=DIRECTION('center_axis',(1.4792020664489E-16,0.,-1.));
#8005=DIRECTION('ref_axis',(-1.,0.,-1.4792020664489E-16));
#8006=DIRECTION('',(0.,1.,0.));
#8007=DIRECTION('',(0.,1.,0.));
#8008=DIRECTION('center_axis',(-0.866025403784439,0.,-0.5));
#8009=DIRECTION('ref_axis',(-0.5,0.,0.866025403784439));
#8010=DIRECTION('',(0.,1.,0.));
#8011=DIRECTION('center_axis',(-0.866025403784439,0.,0.5));
#8012=DIRECTION('ref_axis',(0.5,0.,0.866025403784439));
#8013=DIRECTION('',(0.,1.,0.));
#8014=DIRECTION('center_axis',(0.,1.,0.));
#8015=DIRECTION('ref_axis',(1.,0.,0.));
#8016=DIRECTION('center_axis',(0.,1.,0.));
#8017=DIRECTION('ref_axis',(1.,0.,0.));
#8018=DIRECTION('',(0.,-1.,0.));
#8019=DIRECTION('center_axis',(0.,1.,0.));
#8020=DIRECTION('ref_axis',(1.,0.,0.));
#8021=DIRECTION('center_axis',(-2.95840413289779E-16,0.,1.));
#8022=DIRECTION('ref_axis',(1.,0.,2.95840413289779E-16));
#8023=DIRECTION('',(0.,1.,0.));
#8024=DIRECTION('center_axis',(0.866025403784439,0.,-0.5));
#8025=DIRECTION('ref_axis',(-0.5,0.,-0.866025403784439));
#8026=DIRECTION('',(0.,1.,0.));
#8027=DIRECTION('center_axis',(0.866025403784439,0.,0.5));
#8028=DIRECTION('ref_axis',(0.5,0.,-0.866025403784439));
#8029=DIRECTION('center_axis',(0.,1.,0.));
#8030=DIRECTION('ref_axis',(1.,0.,0.));
#8031=DIRECTION('center_axis',(0.,1.,0.));
#8032=DIRECTION('ref_axis',(1.,0.,0.));
#9611=CARTESIAN_POINT('',(0.,0.,0.));
#9612=CARTESIAN_POINT('Origin',(0.,0.067277284513851,0.));
#9613=CARTESIAN_POINT('',(-0.375277674973257,0.0768195421087395,0.65));
#9614=CARTESIAN_POINT('',(0.375277674973257,0.0768195421087395,0.65));
#9615=CARTESIAN_POINT('Ctrl Pts',(-0.375277674973257,0.0768195421087395,
0.65));
#9616=CARTESIAN_POINT('Ctrl Pts',(1.66533453693773E-13,-0.0315137912242439,
0.65));
#9617=CARTESIAN_POINT('Ctrl Pts',(0.375277674973257,0.0768195421087394,
0.65));
#9618=CARTESIAN_POINT('',(-0.750555349946514,0.0768195421087394,-9.19165206894919E-17));
#9619=CARTESIAN_POINT('Ctrl Pts',(-0.750555349946514,0.0768195421087394,
-9.19165206894919E-17));
#9620=CARTESIAN_POINT('Ctrl Pts',(-0.562916512459802,-0.0315137912242434,
0.325000000000144));
#9621=CARTESIAN_POINT('Ctrl Pts',(-0.375277674973257,0.0768195421087395,
0.65));
#9622=CARTESIAN_POINT('',(-0.6175,-2.77555756156289E-17,-7.5621939847349E-17));
#9623=CARTESIAN_POINT('',(-0.734027674973257,0.067277284513851,-8.98924642641573E-17));
#9624=CARTESIAN_POINT('Origin',(0.,0.,0.));
#9625=CARTESIAN_POINT('',(-0.375277674973257,0.0768195421087395,-0.65));
#9626=CARTESIAN_POINT('Ctrl Pts',(-0.375277674973257,0.0768195421087395,
-0.65));
#9627=CARTESIAN_POINT('Ctrl Pts',(-0.562916512459968,-0.0315137912242437,
-0.324999999999856));
#9628=CARTESIAN_POINT('Ctrl Pts',(-0.750555349946514,0.0768195421087395,
-9.19165206894919E-17));
#9629=CARTESIAN_POINT('',(0.375277674973257,0.0768195421087395,-0.65));
#9630=CARTESIAN_POINT('Ctrl Pts',(0.375277674973257,0.0768195421087395,
-0.65));
#9631=CARTESIAN_POINT('Ctrl Pts',(-1.66144875635155E-13,-0.0315137912242437,
-0.65));
#9632=CARTESIAN_POINT('Ctrl Pts',(-0.375277674973257,0.0768195421087395,
-0.65));
#9633=CARTESIAN_POINT('',(0.750555349946514,0.0768195421087394,0.));
#9634=CARTESIAN_POINT('Ctrl Pts',(0.750555349946514,0.0768195421087394,
0.));
#9635=CARTESIAN_POINT('Ctrl Pts',(0.562916512459802,-0.0315137912242436,
-0.325000000000144));
#9636=CARTESIAN_POINT('Ctrl Pts',(0.375277674973257,0.0768195421087395,
-0.65));
#9637=CARTESIAN_POINT('Ctrl Pts',(0.375277674973257,0.0768195421087394,
0.65));
#9638=CARTESIAN_POINT('Ctrl Pts',(0.562916512459968,-0.0315137912242439,
0.324999999999856));
#9639=CARTESIAN_POINT('Ctrl Pts',(0.750555349946514,0.0768195421087394,
0.));
#9640=CARTESIAN_POINT('Origin',(0.,0.612722715486149,0.));
#9641=CARTESIAN_POINT('',(-0.6175,0.68,-7.5621939847349E-17));
#9642=CARTESIAN_POINT('Origin',(0.,0.68,0.));
#9643=CARTESIAN_POINT('',(-0.750555349946514,0.603180457891261,-9.19165206894919E-17));
#9644=CARTESIAN_POINT('',(-0.734027674973257,0.612722715486149,-8.98924642641573E-17));
#9645=CARTESIAN_POINT('',(-0.375277674973257,0.603180457891261,0.65));
#9646=CARTESIAN_POINT('Ctrl Pts',(-0.375277674973257,0.603180457891261,
0.65));
#9647=CARTESIAN_POINT('Ctrl Pts',(-0.562916512459968,0.711513791224243,
0.324999999999856));
#9648=CARTESIAN_POINT('Ctrl Pts',(-0.750555349946514,0.603180457891261,
-9.19165206894919E-17));
#9649=CARTESIAN_POINT('',(0.375277674973257,0.603180457891261,0.65));
#9650=CARTESIAN_POINT('Ctrl Pts',(0.375277674973257,0.603180457891261,0.65));
#9651=CARTESIAN_POINT('Ctrl Pts',(-1.66755498298699E-13,0.711513791224244,
0.65));
#9652=CARTESIAN_POINT('Ctrl Pts',(-0.375277674973257,0.603180457891261,
0.65));
#9653=CARTESIAN_POINT('',(0.750555349946514,0.603180457891261,0.));
#9654=CARTESIAN_POINT('Ctrl Pts',(0.750555349946514,0.603180457891261,0.));
#9655=CARTESIAN_POINT('Ctrl Pts',(0.562916512459802,0.711513791224244,0.325000000000144));
#9656=CARTESIAN_POINT('Ctrl Pts',(0.375277674973257,0.603180457891261,0.65));
#9657=CARTESIAN_POINT('',(0.375277674973257,0.603180457891261,-0.65));
#9658=CARTESIAN_POINT('Ctrl Pts',(0.375277674973257,0.603180457891261,-0.65));
#9659=CARTESIAN_POINT('Ctrl Pts',(0.562916512459969,0.711513791224244,-0.324999999999856));
#9660=CARTESIAN_POINT('Ctrl Pts',(0.750555349946514,0.603180457891261,0.));
#9661=CARTESIAN_POINT('',(-0.375277674973257,0.603180457891261,-0.65));
#9662=CARTESIAN_POINT('Ctrl Pts',(-0.375277674973257,0.603180457891261,
-0.65));
#9663=CARTESIAN_POINT('Ctrl Pts',(1.66422431391311E-13,0.711513791224244,
-0.65));
#9664=CARTESIAN_POINT('Ctrl Pts',(0.375277674973257,0.603180457891261,-0.65));
#9665=CARTESIAN_POINT('Ctrl Pts',(-0.750555349946514,0.603180457891261,
-9.19165206894919E-17));
#9666=CARTESIAN_POINT('Ctrl Pts',(-0.562916512459802,0.711513791224244,
-0.325000000000144));
#9667=CARTESIAN_POINT('Ctrl Pts',(-0.375277674973257,0.603180457891261,
-0.65));
#9668=CARTESIAN_POINT('Origin',(0.375277674973257,0.,-0.65));
#9669=CARTESIAN_POINT('',(-0.375277674973257,0.,-0.65));
#9670=CARTESIAN_POINT('',(0.375277674973257,0.,-0.65));
#9671=CARTESIAN_POINT('Origin',(-0.375277674973257,0.,-0.65));
#9672=CARTESIAN_POINT('',(-0.750555349946514,0.,-9.19165206894919E-17));
#9673=CARTESIAN_POINT('Origin',(-0.750555349946514,0.,-9.19165206894919E-17));
#9674=CARTESIAN_POINT('',(-0.375277674973257,0.,0.65));
#9675=CARTESIAN_POINT('Origin',(0.,0.,0.));
#9676=CARTESIAN_POINT('',(-0.338975,0.68,4.15124648740974E-17));
#9677=CARTESIAN_POINT('Origin',(0.,0.68,0.));
#9678=CARTESIAN_POINT('',(-0.338975,0.,4.15124648740974E-17));
#9679=CARTESIAN_POINT('',(-0.338975,0.,4.15124648740974E-17));
#9680=CARTESIAN_POINT('Origin',(0.,0.,0.));
#9681=CARTESIAN_POINT('Origin',(-0.375277674973257,0.,0.65));
#9682=CARTESIAN_POINT('',(0.375277674973257,0.,0.65));
#9683=CARTESIAN_POINT('Origin',(0.750555349946514,0.,0.));
#9684=CARTESIAN_POINT('',(0.750555349946514,0.,0.));
#9685=CARTESIAN_POINT('Origin',(0.375277674973257,0.,0.65));
#9686=CARTESIAN_POINT('Origin',(0.,0.68,-1.11022302462516E-16));
#9687=CARTESIAN_POINT('Origin',(0.,0.,-1.11022302462516E-16));
#10050=UNCERTAINTY_MEASURE_WITH_UNIT(LENGTH_MEASURE(0.001),#10096,
'DISTANCE_ACCURACY_VALUE',
'Maximum model space distance between geometric entities at asserted c
onnectivities');
#10058=UNCERTAINTY_MEASURE_WITH_UNIT(LENGTH_MEASURE(0.001),#10096,
'DISTANCE_ACCURACY_VALUE',
'Maximum model space distance between geometric entities at asserted c
onnectivities');
#10087=(
GEOMETRIC_REPRESENTATION_CONTEXT(3)
GLOBAL_UNCERTAINTY_ASSIGNED_CONTEXT((#10050))
GLOBAL_UNIT_ASSIGNED_CONTEXT((#10096,#10098,#10099))
REPRESENTATION_CONTEXT('','3D')
);
#10095=(
GEOMETRIC_REPRESENTATION_CONTEXT(3)
GLOBAL_UNCERTAINTY_ASSIGNED_CONTEXT((#10058))
GLOBAL_UNIT_ASSIGNED_CONTEXT((#10096,#10098,#10099))
REPRESENTATION_CONTEXT('','3D')
);
#10096=(
LENGTH_UNIT()
NAMED_UNIT(*)
SI_UNIT(.CENTI.,.METRE.)
);
#10098=(
NAMED_UNIT(*)
PLANE_ANGLE_UNIT()
SI_UNIT($,.RADIAN.)
);
#10099=(
NAMED_UNIT(*)
SI_UNIT($,.STERADIAN.)
SOLID_ANGLE_UNIT()
);
#10128=SHAPE_DEFINITION_REPRESENTATION(#10199,#10275);
#10199=PRODUCT_DEFINITION_SHAPE('',$,#10312);
#10275=SHAPE_REPRESENTATION('',(#6460),#10087);
#10283=PRODUCT_DEFINITION_CONTEXT('part definition',#10393,'design');
#10312=PRODUCT_DEFINITION('Hex Nut - M8','Hex Nut - M8',#10348,#10283);
#10348=PRODUCT_DEFINITION_FORMATION('',$,#10423);
#10393=APPLICATION_CONTEXT(
'Core Data for Automotive Mechanical Design Process');
#10394=PRODUCT_CONTEXT('part definition',#10393,'mechanical');
#10423=PRODUCT('Hex Nut - M8','Hex Nut - M8','Hex Nut - M8',(#10394));
#10501=COLOUR_RGB('Black',0.12,0.14,0.17);
#10502=FILL_AREA_STYLE_COLOUR('',#10501);
#10503=FILL_AREA_STYLE('',(#10502));
#10504=SURFACE_STYLE_FILL_AREA(#10503);
#10505=SURFACE_SIDE_STYLE('',(#10504));
#10506=SURFACE_STYLE_USAGE(.BOTH.,#10505);
#10507=PRESENTATION_STYLE_ASSIGNMENT((#10506));
ENDSEC;
END-ISO-10303-21;
